ISO-10303-21;
HEADER;
FILE_DESCRIPTION (('STEP AP214'),
    '1' );
FILE_NAME ('socket head cap screw_iso_ISO 4762 M5 x 12 - 12N.step',
    '2026-10-31T03:46:07',
    ( '' ),
    ( '' ),
    'SwSTEP 2.0',
    'SolidWorks 2026',
    '' );
FILE_SCHEMA (( 'AUTOMOTIVE_DESIGN' ));
ENDSEC;

DATA;
#21=CARTESIAN_POINT ( 'NONE',  ( -31.74999999999995737, 0.000000000000000000, 4.250000000000000000 ) ) ;
#38=SURFACE_SIDE_STYLE ('',( #3514 ) ) ;
#106=ORIENTED_EDGE ( 'NONE', *, *, #18345, .F. ) ;
#127=CARTESIAN_POINT ( 'NONE',  ( 2.500000000000000000, 1.178949249685213863, -2.042000000000001148 ) ) ;
#145=CARTESIAN_POINT ( 'NONE',  ( 5.200000000000002842, 0.000000000000000000, 0.000000000000000000 ) ) ;
#148=CIRCLE ( 'NONE', #12147, 2.700000000000000622 ) ;
#195=EDGE_LOOP ( 'NONE', ( #21497, #11165, #16158, #18596 ) ) ;
#230=CARTESIAN_POINT ( 'NONE',  ( 0.2500000000000002220, 0.000000000000000000, 0.000000000000000000 ) ) ;
#282=CARTESIAN_POINT ( 'NONE',  ( 2.500000000000000000, 1.178949249685213863, -2.042000000000001148 ) ) ;
#319=AXIS2_PLACEMENT_3D ( 'NONE', #13284, #11460, #20592 ) ;
#335=CARTESIAN_POINT ( 'NONE',  ( 2.500000000000000000, 1.768423874527824902, 1.020999999999999019 ) ) ;
#339=CARTESIAN_POINT ( 'NONE',  ( 2.500000000000000000, 2.357898499370433054, -1.951563910473907981E-15 ) ) ;
#409=CARTESIAN_POINT ( 'NONE',  ( 2.500000000000000000, -2.357898499370432610, 3.252606517456513302E-15 ) ) ;
#540=CARTESIAN_POINT ( 'NONE',  ( 2.500000000000000000, 2.357898499370433054, -1.951563910473907981E-15 ) ) ;
#543=EDGE_LOOP ( 'NONE', ( #6408, #4802, #11435, #2542 ) ) ;
#578=FACE_OUTER_BOUND ( 'NONE', #18911, .T. ) ;
#616=ADVANCED_FACE ( 'NONE', ( #7814 ), #9512, .F. ) ;
#627=ORIENTED_EDGE ( 'NONE', *, *, #7371, .F. ) ;
#660=ORIENTED_EDGE ( 'NONE', *, *, #11816, .T. ) ;
#682=CARTESIAN_POINT ( 'NONE',  ( 0.000000000000000000, 1.178949249685218525, 2.041999999999999371 ) ) ;
#698=CARTESIAN_POINT ( 'NONE',  ( -31.74999999999995737, 0.000000000000000000, 2.500000000000000444 ) ) ;
#740=CIRCLE ( 'NONE', #10410, 2.041999999999999815 ) ;
#795=LINE ( 'NONE', #16220, #3817 ) ;
#804=ORIENTED_EDGE ( 'NONE', *, *, #13825, .T. ) ;
#844=CARTESIAN_POINT ( 'NONE',  ( 0.000000000000000000, 0.000000000000000000, 4.000000000000000000 ) ) ;
#865=DIRECTION ( 'NONE',  ( 0.000000000000000000, 0.000000000000000000, -1.000000000000000000 ) ) ;
#866=AXIS2_PLACEMENT_3D ( 'NONE', #22309, #11621, #11359 ) ;
#868=ORIENTED_EDGE ( 'NONE', *, *, #19695, .F. ) ;
#874=VERTEX_POINT ( 'NONE', #16724 ) ;
#889=DIRECTION ( 'NONE',  ( 0.000000000000000000, 0.000000000000000000, 1.000000000000000000 ) ) ;
#920=CARTESIAN_POINT ( 'NONE',  ( 0.000000000000000000, -1.178949249685213863, 2.042000000000002924 ) ) ;
#987=AXIS2_PLACEMENT_3D ( 'NONE', #1859, #16486, #13027 ) ;
#1027=FACE_OUTER_BOUND ( 'NONE', #543, .T. ) ;
#1037=CARTESIAN_POINT ( 'NONE',  ( 2.500000000000000000, 2.357898499370433054, -1.951563910473907981E-15 ) ) ;
#1044=DIRECTION ( 'NONE',  ( 0.000000000000000000, 1.224646799147353207E-16, 1.000000000000000000 ) ) ;
#1127=VERTEX_POINT ( 'NONE', #1331 ) ;
#1138=LINE ( 'NONE', #23699, #20177 ) ;
#1158=DIRECTION ( 'NONE',  ( 0.000000000000000000, 0.000000000000000000, -1.000000000000000000 ) ) ;
#1249=LINE ( 'NONE', #12167, #2291 ) ;
#1329=AXIS2_PLACEMENT_3D ( 'NONE', #9733, #11807, #22623 ) ;
#1331=CARTESIAN_POINT ( 'NONE',  ( 0.2500000000000002220, 5.204748896376250699E-16, -4.250000000000000000 ) ) ;
#1332=VECTOR ( 'NONE', #19926, 1000.000000000000000 ) ;
#1336=EDGE_CURVE ( 'NONE', #3845, #2034, #5803, .T. ) ;
#1401=DIRECTION ( 'NONE',  ( -1.000000000000000000, -0.000000000000000000, -0.000000000000000000 ) ) ;
#1414=CARTESIAN_POINT ( 'NONE',  ( 2.500000000000000000, -2.357898499370432610, 3.252606517456513302E-15 ) ) ;
#1437=ORIENTED_EDGE ( 'NONE', *, *, #10670, .F. ) ;
#1446=AXIS2_PLACEMENT_3D ( 'NONE', #145, #7865, #14889 ) ;
#1477=CARTESIAN_POINT ( 'NONE',  ( -31.74999999999995737, 3.061616997868383634E-16, -2.500000000000000444 ) ) ;
#1641=CARTESIAN_POINT ( 'NONE',  ( 0.2500000000000002220, 0.000000000000000000, 0.000000000000000000 ) ) ;
#1659=ORIENTED_EDGE ( 'NONE', *, *, #3677, .T. ) ;
#1669=ORIENTED_EDGE ( 'NONE', *, *, #7701, .T. ) ;
#1713=EDGE_LOOP ( 'NONE', ( #20461, #7584, #11556, #5521, #1659 ) ) ;
#1720=AXIS2_PLACEMENT_3D ( 'NONE', #3933, #5997, #18550 ) ;
#1730=ORIENTED_EDGE ( 'NONE', *, *, #1871, .F. ) ;
#1751=FACE_OUTER_BOUND ( 'NONE', #21991, .T. ) ;
#1776=CARTESIAN_POINT ( 'NONE',  ( 2.500000000000000000, 2.357898499370433054, -1.951563910473907981E-15 ) ) ;
#1781=SHAPE_DEFINITION_REPRESENTATION ( #5553, #18083 ) ;
#1816=VERTEX_POINT ( 'NONE', #16868 ) ;
#1821=VERTEX_POINT ( 'NONE', #7699 ) ;
#1837=DIRECTION ( 'NONE',  ( 0.000000000000000000, 1.000000000000000000, -1.287488025362403787E-15 ) ) ;
#1859=CARTESIAN_POINT ( 'NONE',  ( 5.200000000000002842, 0.000000000000000000, 0.000000000000000000 ) ) ;
#1871=EDGE_CURVE ( 'NONE', #12413, #8456, #8408, .T. ) ;
#1930=CARTESIAN_POINT ( 'NONE',  ( 17.00000000000000000, 2.789133085058097101E-16, -2.055000000000000160 ) ) ;
#1969=DIRECTION ( 'NONE',  ( 0.000000000000000000, 0.8660254037844380415, -0.5000000000000012212 ) ) ;
#2034=VERTEX_POINT ( 'NONE', #7174 ) ;
#2048=CARTESIAN_POINT ( 'NONE',  ( 2.500000000000000000, 2.357898499370433054, -1.951563910473907981E-15 ) ) ;
#2089=CARTESIAN_POINT ( 'NONE',  ( 5.000000000000000888, 0.000000000000000000, 0.000000000000000000 ) ) ;
#2106=DIRECTION ( 'NONE',  ( -1.000000000000000000, -0.000000000000000000, -0.000000000000000000 ) ) ;
#2124=AXIS2_PLACEMENT_3D ( 'NONE', #339, #11607, #2613 ) ;
#2142=TOROIDAL_SURFACE ( 'NONE', #987, 2.700000000000000622, 0.2000000000000000111 ) ;
#2144=ORIENTED_EDGE ( 'NONE', *, *, #17878, .T. ) ;
#2167=FACE_OUTER_BOUND ( 'NONE', #8850, .T. ) ;
#2204=DIRECTION ( 'NONE',  ( -1.000000000000000000, -0.000000000000000000, -0.000000000000000000 ) ) ;
#2217=DIRECTION ( 'NONE',  ( -1.000000000000000000, -0.000000000000000000, -0.000000000000000000 ) ) ;
#2247=DIRECTION ( 'NONE',  ( 1.000000000000000000, 0.000000000000000000, 0.000000000000000000 ) ) ;
#2248=AXIS2_PLACEMENT_3D ( 'NONE', #11280, #20061, #7381 ) ;
#2254=ORIENTED_EDGE ( 'NONE', *, *, #5482, .F. ) ;
#2266=CIRCLE ( 'NONE', #12366, 4.000000000000000000 ) ;
#2291=VECTOR ( 'NONE', #8624, 1000.000000000000000 ) ;
#2323=VERTEX_POINT ( 'NONE', #21411 ) ;
#2342=LINE ( 'NONE', #540, #13059 ) ;
#2344=CARTESIAN_POINT ( 'NONE',  ( 2.500000000000000000, -1.178949249685218303, -2.041999999999998039 ) ) ;
#2387=FACE_OUTER_BOUND ( 'NONE', #12160, .T. ) ;
#2498=LINE ( 'NONE', #4057, #10658 ) ;
#2537=VERTEX_POINT ( 'NONE', #9226 ) ;
#2542=ORIENTED_EDGE ( 'NONE', *, *, #13946, .F. ) ;
#2613=DIRECTION ( 'NONE',  ( 0.000000000000000000, 0.000000000000000000, -1.000000000000000000 ) ) ;
#2627=DIRECTION ( 'NONE',  ( 0.000000000000000000, 0.000000000000000000, 1.000000000000000000 ) ) ;
#2642=FACE_OUTER_BOUND ( 'NONE', #20715, .T. ) ;
#2649=MECHANICAL_DESIGN_GEOMETRIC_PRESENTATION_REPRESENTATION('',(#17334),#12363);
#2707=ORIENTED_EDGE ( 'NONE', *, *, #6136, .F. ) ;
#2714=CIRCLE ( 'NONE', #18909, 2.500000000000000444 ) ;
#2769=ORIENTED_EDGE ( 'NONE', *, *, #12380, .F. ) ;
#2847=ORIENTED_EDGE ( 'NONE', *, *, #6643, .T. ) ;
#2916=LINE ( 'NONE', #14077, #12237 ) ;
#2956=FACE_OUTER_BOUND ( 'NONE', #16526, .T. ) ;
#2980=DIRECTION ( 'NONE',  ( -1.000000000000000000, -0.000000000000000000, -0.000000000000000000 ) ) ;
#3033=ORIENTED_EDGE ( 'NONE', *, *, #15822, .F. ) ;
#3047=ORIENTED_EDGE ( 'NONE', *, *, #12437, .T. ) ;
#3056=ORIENTED_EDGE ( 'NONE', *, *, #23066, .F. ) ;
#3080=VERTEX_POINT ( 'NONE', #13894 ) ;
#3109=EDGE_LOOP ( 'NONE', ( #20326, #20107, #3159, #5201, #14814, #19397 ) ) ;
#3159=ORIENTED_EDGE ( 'NONE', *, *, #18614, .T. ) ;
#3166=DIRECTION ( 'NONE',  ( 0.000000000000000000, -0.5000000000000012212, -0.8660254037844380415 ) ) ;
#3220=DIRECTION ( 'NONE',  ( 0.000000000000000000, 0.000000000000000000, 1.000000000000000000 ) ) ;
#3232=CARTESIAN_POINT ( 'NONE',  ( 5.000000000000000888, 0.000000000000000000, 0.000000000000000000 ) ) ;
#3249=ORIENTED_EDGE ( 'NONE', *, *, #12437, .F. ) ;
#3306=DIRECTION ( 'NONE',  ( 0.000000000000000000, -1.000000000000000000, 1.287488025362403787E-15 ) ) ;
#3321=CARTESIAN_POINT ( 'NONE',  ( 2.500000000000000000, 0.000000000000000000, 0.000000000000000000 ) ) ;
#3338=DIRECTION ( 'NONE',  ( 0.000000000000000000, -0.4999999999999992784, 0.8660254037844389297 ) ) ;
#3362=ORIENTED_EDGE ( 'NONE', *, *, #21394, .F. ) ;
#3423=( GEOMETRIC_REPRESENTATION_CONTEXT ( 3 ) GLOBAL_UNCERTAINTY_ASSIGNED_CONTEXT ( ( #20728 ) ) GLOBAL_UNIT_ASSIGNED_CONTEXT ( ( #18486, #22097, #20411 ) ) REPRESENTATION_CONTEXT ( 'NONE', 'WORKASPACE' ) );
#3506=ADVANCED_FACE ( 'NONE', ( #1027 ), #4976, .T. ) ;
#3514=SURFACE_STYLE_FILL_AREA ( #16686 ) ;
#3568=DIRECTION ( 'NONE',  ( -0.000000000000000000, 0.8660254037844390407, 0.4999999999999993339 ) ) ;
#3603=ORIENTED_EDGE ( 'NONE', *, *, #7494, .T. ) ;
#3616=SHAPE_REPRESENTATION_RELATIONSHIP ( 'NONE' , 'NONE' ,  #18083, #7558 ) ;
#3629=LINE ( 'NONE', #1477, #13456 ) ;
#3635=ORIENTED_EDGE ( 'NONE', *, *, #3677, .F. ) ;
#3677=EDGE_CURVE ( 'NONE', #2034, #5659, #4394, .T. ) ;
#3705=CARTESIAN_POINT ( 'NONE',  ( 16.55500000000001393, 3.061616997868383634E-16, -2.500000000000000444 ) ) ;
#3769=DIRECTION ( 'NONE',  ( 1.000000000000000000, 0.000000000000000000, 0.000000000000000000 ) ) ;
#3776=VECTOR ( 'NONE', #18332, 1000.000000000000000 ) ;
#3797=EDGE_CURVE ( 'NONE', #12879, #9739, #1249, .T. ) ;
#3817=VECTOR ( 'NONE', #22769, 1000.000000000000000 ) ;
#3838=( GEOMETRIC_REPRESENTATION_CONTEXT ( 3 ) GLOBAL_UNCERTAINTY_ASSIGNED_CONTEXT ( ( #13553 ) ) GLOBAL_UNIT_ASSIGNED_CONTEXT ( ( #9334, #14883, #5218 ) ) REPRESENTATION_CONTEXT ( 'NONE', 'WORKASPACE' ) );
#3845=VERTEX_POINT ( 'NONE', #12524 ) ;
#3860=AXIS2_PLACEMENT_3D ( 'NONE', #9773, #9408, #22665 ) ;
#3900=DIRECTION ( 'NONE',  ( 0.000000000000000000, 0.5000000000000012212, 0.8660254037844380415 ) ) ;
#3917=FACE_OUTER_BOUND ( 'NONE', #19588, .T. ) ;
#3933=CARTESIAN_POINT ( 'NONE',  ( 2.500000000000000000, 2.357898499370433054, -1.951563910473907981E-15 ) ) ;
#4057=CARTESIAN_POINT ( 'NONE',  ( -31.74999999999995737, 5.204748896376250699E-16, -4.250000000000000000 ) ) ;
#4101=DIRECTION ( 'NONE',  ( 0.000000000000000000, 0.000000000000000000, 1.000000000000000000 ) ) ;
#4155=CARTESIAN_POINT ( 'NONE',  ( -31.74999999999995737, 0.000000000000000000, 0.000000000000000000 ) ) ;
#4201=AXIS2_PLACEMENT_3D ( 'NONE', #5217, #18484, #20064 ) ;
#4286=ADVANCED_FACE ( 'NONE', ( #5092 ), #18131, .T. ) ;
#4292=EDGE_CURVE ( 'NONE', #7788, #14717, #23562, .T. ) ;
#4321=CARTESIAN_POINT ( 'NONE',  ( 17.00000000000000000, 0.000000000000000000, 2.055000000000000160 ) ) ;
#4347=DIRECTION ( 'NONE',  ( -1.000000000000000000, 0.000000000000000000, -0.000000000000000000 ) ) ;
#4360=DIRECTION ( 'NONE',  ( 0.000000000000000000, -0.4999999999999993894, 0.8660254037844389297 ) ) ;
#4394=LINE ( 'NONE', #2344, #13542 ) ;
#4449=ORIENTED_EDGE ( 'NONE', *, *, #15655, .T. ) ;
#4498=CARTESIAN_POINT ( 'NONE',  ( 2.500000000000000000, 2.357898499370433054, -1.951563910473907981E-15 ) ) ;
#4540=CIRCLE ( 'NONE', #1446, 2.500000000000000444 ) ;
#4554=ADVANCED_FACE ( 'NONE', ( #2642 ), #15941, .F. ) ;
#4562=CARTESIAN_POINT ( 'NONE',  ( 2.500000000000000000, -1.178949249685213863, 2.042000000000002924 ) ) ;
#4679=DIRECTION ( 'NONE',  ( 0.000000000000000000, 0.000000000000000000, -1.000000000000000000 ) ) ;
#4767=AXIS2_PLACEMENT_3D ( 'NONE', #6937, #10335, #17811 ) ;
#4802=ORIENTED_EDGE ( 'NONE', *, *, #11282, .T. ) ;
#4843=AXIS2_PLACEMENT_3D ( 'NONE', #21224, #6477, #4679 ) ;
#4851=ADVANCED_FACE ( 'NONE', ( #15413 ), #22977, .T. ) ;
#4855=DIRECTION ( 'NONE',  ( 0.000000000000000000, -0.8660254037844390407, -0.4999999999999994449 ) ) ;
#4916=LINE ( 'NONE', #1037, #16969 ) ;
#4953=ORIENTED_EDGE ( 'NONE', *, *, #15655, .F. ) ;
#4976=CONICAL_SURFACE ( 'NONE', #16179, 2.055000000000000160, 0.7853981633974633780 ) ;
#4978=CYLINDRICAL_SURFACE ( 'NONE', #6537, 4.250000000000000000 ) ;
#5016=LINE ( 'NONE', #21069, #19220 ) ;
#5049=DIRECTION ( 'NONE',  ( 0.000000000000000000, -0.4999999999999993894, 0.8660254037844389297 ) ) ;
#5054=ADVANCED_FACE ( 'NONE', ( #11063 ), #14794, .F. ) ;
#5092=FACE_OUTER_BOUND ( 'NONE', #8733, .T. ) ;
#5158=DIRECTION ( 'NONE',  ( -1.000000000000000000, -0.000000000000000000, -0.000000000000000000 ) ) ;
#5165=AXIS2_PLACEMENT_3D ( 'NONE', #6280, #6639, #19061 ) ;
#5201=ORIENTED_EDGE ( 'NONE', *, *, #8482, .T. ) ;
#5207=DIRECTION ( 'NONE',  ( 0.000000000000000000, 0.000000000000000000, -1.000000000000000000 ) ) ;
#5217=CARTESIAN_POINT ( 'NONE',  ( 0.2500000000000002220, 4.898587196589412829E-16, -4.000000000000000000 ) ) ;
#5218=( NAMED_UNIT ( * ) SI_UNIT ( $, .STERADIAN. ) SOLID_ANGLE_UNIT ( ) );
#5275=PLANE ( 'NONE',  #7839 ) ;
#5291=EDGE_CURVE ( 'NONE', #10553, #13555, #8137, .T. ) ;
#5313=AXIS2_PLACEMENT_3D ( 'NONE', #6856, #2980, #3220 ) ;
#5424=DIRECTION ( 'NONE',  ( 0.000000000000000000, -0.4999999999999993894, 0.8660254037844389297 ) ) ;
#5482=EDGE_CURVE ( 'NONE', #11930, #11372, #18883, .T. ) ;
#5495=ORIENTED_EDGE ( 'NONE', *, *, #6369, .T. ) ;
#5521=ORIENTED_EDGE ( 'NONE', *, *, #7371, .T. ) ;
#5553=PRODUCT_DEFINITION_SHAPE ( 'NONE', 'NONE',  #16409 ) ;
#5578=ORIENTED_EDGE ( 'NONE', *, *, #12380, .T. ) ;
#5616=AXIS2_PLACEMENT_3D ( 'NONE', #3321, #17949, #18067 ) ;
#5617=CARTESIAN_POINT ( 'NONE',  ( 0.000000000000000000, -1.178949249685213863, 2.042000000000002924 ) ) ;
#5625=CARTESIAN_POINT ( 'NONE',  ( 2.500000000000000000, 2.357898499370433054, -1.951563910473907981E-15 ) ) ;
#5659=VERTEX_POINT ( 'NONE', #22568 ) ;
#5687=FILL_AREA_STYLE_COLOUR ( '', #17365 ) ;
#5741=AXIS2_PLACEMENT_3D ( 'NONE', #21707, #23271, #15365 ) ;
#5744=VECTOR ( 'NONE', #6375, 1000.000000000000114 ) ;
#5803=LINE ( 'NONE', #22683, #22575 ) ;
#5820=DIRECTION ( 'NONE',  ( 0.000000000000000000, 0.000000000000000000, -1.000000000000000000 ) ) ;
#5840=PLANE ( 'NONE',  #11770 ) ;
#5845=DIRECTION ( 'NONE',  ( -1.000000000000000000, -0.000000000000000000, -0.000000000000000000 ) ) ;
#5862=DIRECTION ( 'NONE',  ( -1.000000000000000000, -0.000000000000000000, -0.000000000000000000 ) ) ;
#5877=ORIENTED_EDGE ( 'NONE', *, *, #19695, .T. ) ;
#5894=LINE ( 'NONE', #698, #17464 ) ;
#5906=ORIENTED_EDGE ( 'NONE', *, *, #11282, .F. ) ;
#5926=CARTESIAN_POINT ( 'NONE',  ( -31.74999999999995737, 0.000000000000000000, 0.000000000000000000 ) ) ;
#5981=CARTESIAN_POINT ( 'NONE',  ( 0.000000000000000000, 0.000000000000000000, 0.000000000000000000 ) ) ;
#5997=DIRECTION ( 'NONE',  ( 1.000000000000000000, 0.000000000000000000, 0.000000000000000000 ) ) ;
#6004=PLANE ( 'NONE',  #2124 ) ;
#6015=ORIENTED_EDGE ( 'NONE', *, *, #18351, .F. ) ;
#6049=ADVANCED_FACE ( 'NONE', ( #2387 ), #19673, .T. ) ;
#6079=DIRECTION ( 'NONE',  ( 0.000000000000000000, 0.000000000000000000, -1.000000000000000000 ) ) ;
#6136=EDGE_CURVE ( 'NONE', #19431, #18385, #2714, .T. ) ;
#6162=ORIENTED_EDGE ( 'NONE', *, *, #3797, .F. ) ;
#6163=FACE_OUTER_BOUND ( 'NONE', #12762, .T. ) ;
#6280=CARTESIAN_POINT ( 'NONE',  ( 0.2500000000000002220, 0.000000000000000000, 0.000000000000000000 ) ) ;
#6290=ORIENTED_EDGE ( 'NONE', *, *, #21599, .F. ) ;
#6303=UNCERTAINTY_MEASURE_WITH_UNIT (LENGTH_MEASURE( 1.000000000000000082E-05 ), #13864, 'distance_accuracy_value', 'NONE');
#6330=FACE_OUTER_BOUND ( 'NONE', #12863, .T. ) ;
#6369=EDGE_CURVE ( 'NONE', #874, #10912, #2266, .T. ) ;
#6375=DIRECTION ( 'NONE',  ( 0.000000000000000000, -0.5000000000000011102, -0.8660254037844379305 ) ) ;
#6408=ORIENTED_EDGE ( 'NONE', *, *, #5482, .T. ) ;
#6456=EDGE_CURVE ( 'NONE', #6907, #23173, #740, .T. ) ;
#6477=DIRECTION ( 'NONE',  ( 1.000000000000000000, 0.000000000000000000, 0.000000000000000000 ) ) ;
#6509=ORIENTED_EDGE ( 'NONE', *, *, #7837, .T. ) ;
#6537=AXIS2_PLACEMENT_3D ( 'NONE', #20951, #19818, #8602 ) ;
#6545=AXIS2_PLACEMENT_3D ( 'NONE', #16289, #23631, #7087 ) ;
#6570=ADVANCED_FACE ( 'NONE', ( #17892 ), #23437, .T. ) ;
#6588=DIRECTION ( 'NONE',  ( 0.000000000000000000, 1.000000000000000000, -1.471414886128461471E-15 ) ) ;
#6635=EDGE_LOOP ( 'NONE', ( #12150, #660 ) ) ;
#6639=DIRECTION ( 'NONE',  ( -1.000000000000000000, -0.000000000000000000, -0.000000000000000000 ) ) ;
#6643=EDGE_CURVE ( 'NONE', #10894, #15982, #795, .T. ) ;
#6663=ADVANCED_FACE ( 'NONE', ( #12508 ), #4978, .T. ) ;
#6820=VERTEX_POINT ( 'NONE', #13221 ) ;
#6856=CARTESIAN_POINT ( 'NONE',  ( 16.55500000000001393, 0.000000000000000000, 0.000000000000000000 ) ) ;
#6907=VERTEX_POINT ( 'NONE', #335 ) ;
#6916=DIRECTION ( 'NONE',  ( 0.000000000000000000, 0.8660254037844380415, -0.5000000000000011102 ) ) ;
#6937=CARTESIAN_POINT ( 'NONE',  ( 5.000000000000004441, 0.000000000000000000, 0.000000000000000000 ) ) ;
#6939=CIRCLE ( 'NONE', #11620, 2.041999999999999815 ) ;
#6963=DIRECTION ( 'NONE',  ( 0.000000000000000000, 0.000000000000000000, 1.000000000000000000 ) ) ;
#7087=DIRECTION ( 'NONE',  ( 0.000000000000000000, 0.000000000000000000, 1.000000000000000000 ) ) ;
#7102=EDGE_CURVE ( 'NONE', #12825, #2537, #7420, .T. ) ;
#7174=CARTESIAN_POINT ( 'NONE',  ( 2.500000000000000000, -1.178949249685218303, -2.041999999999998039 ) ) ;
#7250=CARTESIAN_POINT ( 'NONE',  ( 17.00000000000000000, 0.000000000000000000, 2.055000000000000160 ) ) ;
#7251=ORIENTED_EDGE ( 'NONE', *, *, #6456, .T. ) ;
#7259=DIRECTION ( 'NONE',  ( 0.000000000000000000, 0.5000000000000011102, 0.8660254037844380415 ) ) ;
#7371=EDGE_CURVE ( 'NONE', #13555, #2034, #8952, .T. ) ;
#7373=CARTESIAN_POINT ( 'NONE',  ( 17.00000000000000000, 2.055000000000000160, 0.000000000000000000 ) ) ;
#7375=ORIENTED_EDGE ( 'NONE', *, *, #4292, .T. ) ;
#7381=DIRECTION ( 'NONE',  ( 0.000000000000000000, 0.000000000000000000, 1.000000000000000000 ) ) ;
#7420=CIRCLE ( 'NONE', #12102, 2.500000000000000444 ) ;
#7462=DIRECTION ( 'NONE',  ( 0.000000000000000000, 0.4999999999999993339, -0.8660254037844390407 ) ) ;
#7467=DIRECTION ( 'NONE',  ( 0.000000000000000000, 0.4999999999999993339, -0.8660254037844390407 ) ) ;
#7481=DIRECTION ( 'NONE',  ( 0.000000000000000000, -1.000000000000000000, 1.287488025362403787E-15 ) ) ;
#7494=EDGE_CURVE ( 'NONE', #18385, #2537, #5894, .T. ) ;
#7519=DIRECTION ( 'NONE',  ( 0.000000000000000000, -1.287488025362403787E-15, -1.000000000000000000 ) ) ;
#7529=ADVANCED_FACE ( 'NONE', ( #18674 ), #11319, .T. ) ;
#7558=ADVANCED_BREP_SHAPE_REPRESENTATION ( '', ( #20059, #11210 ), #3838 ) ;
#7564=EDGE_CURVE ( 'NONE', #1816, #7788, #13651, .T. ) ;
#7584=ORIENTED_EDGE ( 'NONE', *, *, #23025, .F. ) ;
#7590=AXIS2_PLACEMENT_3D ( 'NONE', #5926, #10163, #4101 ) ;
#7629=AXIS2_PLACEMENT_3D ( 'NONE', #11330, #2106, #9498 ) ;
#7699=CARTESIAN_POINT ( 'NONE',  ( 0.000000000000000000, 2.357898499370433054, -1.951563910473907981E-15 ) ) ;
#7701=EDGE_CURVE ( 'NONE', #8456, #6907, #11741, .T. ) ;
#7729=ADVANCED_FACE ( 'NONE', ( #18413, #1751 ), #5275, .T. ) ;
#7788=VERTEX_POINT ( 'NONE', #9128 ) ;
#7814=FACE_OUTER_BOUND ( 'NONE', #8230, .T. ) ;
#7837=EDGE_CURVE ( 'NONE', #14717, #10912, #10165, .T. ) ;
#7839=AXIS2_PLACEMENT_3D ( 'NONE', #17961, #23737, #19881 ) ;
#7865=DIRECTION ( 'NONE',  ( 1.000000000000000000, 0.000000000000000000, 0.000000000000000000 ) ) ;
#8028=DIRECTION ( 'NONE',  ( -1.000000000000000000, -0.000000000000000000, -0.000000000000000000 ) ) ;
#8041=CARTESIAN_POINT ( 'NONE',  ( 2.500000000000000000, 2.357898499370433054, -1.951563910473907981E-15 ) ) ;
#8062=ORIENTED_EDGE ( 'NONE', *, *, #18614, .F. ) ;
#8102=VECTOR ( 'NONE', #7481, 1000.000000000000000 ) ;
#8137=LINE ( 'NONE', #409, #21054 ) ;
#8181=CARTESIAN_POINT ( 'NONE',  ( 2.500000000000000000, -1.178949249685213863, 2.042000000000002924 ) ) ;
#8230=EDGE_LOOP ( 'NONE', ( #19614, #3056, #18369 ) ) ;
#8280=ADVANCED_FACE ( 'NONE', ( #20771 ), #13589, .T. ) ;
#8291=ORIENTED_EDGE ( 'NONE', *, *, #21394, .T. ) ;
#8302=DIRECTION ( 'NONE',  ( 0.000000000000000000, -0.5000000000000011102, -0.8660254037844379305 ) ) ;
#8393=VERTEX_POINT ( 'NONE', #23418 ) ;
#8400=ORIENTED_EDGE ( 'NONE', *, *, #21599, .T. ) ;
#8408=LINE ( 'NONE', #10356, #13091 ) ;
#8456=VERTEX_POINT ( 'NONE', #10902 ) ;
#8482=EDGE_CURVE ( 'NONE', #6820, #5659, #18226, .T. ) ;
#8496=AXIS2_PLACEMENT_3D ( 'NONE', #11028, #20404, #18350 ) ;
#8528=LINE ( 'NONE', #15899, #15038 ) ;
#8602=DIRECTION ( 'NONE',  ( 0.000000000000000000, 0.000000000000000000, 1.000000000000000000 ) ) ;
#8624=DIRECTION ( 'NONE',  ( -1.000000000000000000, -0.000000000000000000, -0.000000000000000000 ) ) ;
#8667=EDGE_CURVE ( 'NONE', #23173, #3845, #17625, .T. ) ;
#8733=EDGE_LOOP ( 'NONE', ( #2254, #9465 ) ) ;
#8835=TOROIDAL_SURFACE ( 'NONE', #5741, 2.700000000000000622, 0.2000000000000000111 ) ;
#8850=EDGE_LOOP ( 'NONE', ( #17006, #868, #12144 ) ) ;
#8877=ORIENTED_EDGE ( 'NONE', *, *, #1336, .F. ) ;
#8904=ORIENTED_EDGE ( 'NONE', *, *, #6369, .F. ) ;
#8952=LINE ( 'NONE', #9307, #11728 ) ;
#8971=ORIENTED_EDGE ( 'NONE', *, *, #10950, .T. ) ;
#9084=SURFACE_STYLE_USAGE ( .BOTH. , #38 ) ;
#9090=PLANE ( 'NONE',  #12687 ) ;
#9093=CIRCLE ( 'NONE', #5616, 2.041999999999999815 ) ;
#9113=CARTESIAN_POINT ( 'NONE',  ( 0.2500000000000002220, 0.000000000000000000, 0.000000000000000000 ) ) ;
#9128=CARTESIAN_POINT ( 'NONE',  ( 5.000000000000004441, 0.000000000000000000, 4.250000000000000000 ) ) ;
#9133=DIRECTION ( 'NONE',  ( 0.000000000000000000, 1.000000000000000000, -1.471414886128461471E-15 ) ) ;
#9139=CARTESIAN_POINT ( 'NONE',  ( 2.500000000000000000, -1.178949249685213863, 2.042000000000002924 ) ) ;
#9148=AXIS2_PLACEMENT_3D ( 'NONE', #13433, #17030, #20747 ) ;
#9226=CARTESIAN_POINT ( 'NONE',  ( 5.200000000000002842, 0.000000000000000000, 2.500000000000000444 ) ) ;
#9300=DIRECTION ( 'NONE',  ( 0.000000000000000000, 0.000000000000000000, -1.000000000000000000 ) ) ;
#9304=PRODUCT_CONTEXT ( 'NONE', #21391, 'mechanical' ) ;
#9307=CARTESIAN_POINT ( 'NONE',  ( 2.500000000000000000, -2.357898499370432610, 3.252606517456513302E-15 ) ) ;
#9322=LINE ( 'NONE', #127, #8102 ) ;
#9334=( LENGTH_UNIT ( ) NAMED_UNIT ( * ) SI_UNIT ( .MILLI., .METRE. ) );
#9357=EDGE_CURVE ( 'NONE', #2323, #5659, #19858, .T. ) ;
#9408=DIRECTION ( 'NONE',  ( -1.000000000000000000, -0.000000000000000000, -0.000000000000000000 ) ) ;
#9415=ORIENTED_EDGE ( 'NONE', *, *, #23066, .T. ) ;
#9465=ORIENTED_EDGE ( 'NONE', *, *, #17171, .F. ) ;
#9473=CARTESIAN_POINT ( 'NONE',  ( 0.000000000000000000, 0.000000000000000000, 0.000000000000000000 ) ) ;
#9498=DIRECTION ( 'NONE',  ( 0.000000000000000000, 0.000000000000000000, 1.000000000000000000 ) ) ;
#9511=FACE_OUTER_BOUND ( 'NONE', #12245, .T. ) ;
#9512=PLANE ( 'NONE',  #1720 ) ;
#9516=EDGE_CURVE ( 'NONE', #3080, #8456, #6939, .T. ) ;
#9529=DIRECTION ( 'NONE',  ( -1.000000000000000000, -0.000000000000000000, -0.000000000000000000 ) ) ;
#9579=EDGE_LOOP ( 'NONE', ( #22910, #106, #19169, #15627, #3047 ) ) ;
#9733=CARTESIAN_POINT ( 'NONE',  ( 2.500000000000000000, 2.357898499370433054, -1.951563910473907981E-15 ) ) ;
#9734=ORIENTED_EDGE ( 'NONE', *, *, #1336, .T. ) ;
#9739=VERTEX_POINT ( 'NONE', #23448 ) ;
#9761=DIRECTION ( 'NONE',  ( 0.000000000000000000, 0.000000000000000000, -1.000000000000000000 ) ) ;
#9773=CARTESIAN_POINT ( 'NONE',  ( 17.00000000000000000, 0.000000000000000000, 0.000000000000000000 ) ) ;
#9860=ORIENTED_EDGE ( 'NONE', *, *, #10950, .F. ) ;
#9931=ADVANCED_FACE ( 'NONE', ( #14378 ), #8835, .F. ) ;
#9985=CIRCLE ( 'NONE', #14238, 0.2000000000000000944 ) ;
#10086=CARTESIAN_POINT ( 'NONE',  ( 2.500000000000000000, -1.768423874527823791, -1.020999999999998353 ) ) ;
#10144=LINE ( 'NONE', #12106, #16210 ) ;
#10163=DIRECTION ( 'NONE',  ( -1.000000000000000000, -0.000000000000000000, -0.000000000000000000 ) ) ;
#10165=CIRCLE ( 'NONE', #23643, 0.2500000000000002220 ) ;
#10242=ORIENTED_EDGE ( 'NONE', *, *, #13825, .F. ) ;
#10335=DIRECTION ( 'NONE',  ( -1.000000000000000000, -0.000000000000000000, -0.000000000000000000 ) ) ;
#10336=( NAMED_UNIT ( * ) SI_UNIT ( $, .STERADIAN. ) SOLID_ANGLE_UNIT ( ) );
#10356=CARTESIAN_POINT ( 'NONE',  ( 2.500000000000000000, 0.000000000000000000, 2.041999999999999815 ) ) ;
#10409=CIRCLE ( 'NONE', #17702, 0.2000000000000000944 ) ;
#10410=AXIS2_PLACEMENT_3D ( 'NONE', #13525, #5862, #18639 ) ;
#10484=EDGE_CURVE ( 'NONE', #12825, #21826, #10409, .T. ) ;
#10492=CARTESIAN_POINT ( 'NONE',  ( 17.00000000000000000, 0.000000000000000000, 0.000000000000000000 ) ) ;
#10498=CYLINDRICAL_SURFACE ( 'NONE', #19041, 2.500000000000000444 ) ;
#10553=VERTEX_POINT ( 'NONE', #12900 ) ;
#10624=VECTOR ( 'NONE', #12966, 1000.000000000000000 ) ;
#10658=VECTOR ( 'NONE', #11351, 1000.000000000000000 ) ;
#10670=EDGE_CURVE ( 'NONE', #21826, #8393, #11194, .T. ) ;
#10703=DIRECTION ( 'NONE',  ( -1.000000000000000000, -0.000000000000000000, -0.000000000000000000 ) ) ;
#10754=AXIS2_PLACEMENT_3D ( 'NONE', #4498, #12040, #865 ) ;
#10873=DIRECTION ( 'NONE',  ( 0.000000000000000000, 0.000000000000000000, 1.000000000000000000 ) ) ;
#10894=VERTEX_POINT ( 'NONE', #22456 ) ;
#10902=CARTESIAN_POINT ( 'NONE',  ( 2.500000000000000000, 3.004629197474318851E-15, 2.042000000000000259 ) ) ;
#10911=DIRECTION ( 'NONE',  ( 1.000000000000000000, 0.000000000000000000, 0.000000000000000000 ) ) ;
#10912=VERTEX_POINT ( 'NONE', #844 ) ;
#10950=EDGE_CURVE ( 'NONE', #12413, #3845, #18399, .T. ) ;
#10966=FACE_OUTER_BOUND ( 'NONE', #195, .T. ) ;
#10969=CARTESIAN_POINT ( 'NONE',  ( -31.74999999999995737, 0.000000000000000000, 0.000000000000000000 ) ) ;
#10988=PRODUCT ( 'socket head cap screw_iso_ISO 4762 M5 x 12 - 12N', 'socket head cap screw_iso_ISO 4762 M5 x 12 - 12N', '', ( #9304 ) ) ;
#11017=PRODUCT_DEFINITION_CONTEXT ( 'detailed design', #19547, 'design' ) ;
#11028=CARTESIAN_POINT ( 'NONE',  ( 17.00000000000000000, 0.000000000000000000, 0.000000000000000000 ) ) ;
#11048=ORIENTED_EDGE ( 'NONE', *, *, #9357, .T. ) ;
#11063=FACE_OUTER_BOUND ( 'NONE', #9579, .T. ) ;
#11071=ORIENTED_EDGE ( 'NONE', *, *, #15826, .T. ) ;
#11165=ORIENTED_EDGE ( 'NONE', *, *, #7102, .F. ) ;
#11182=ADVANCED_FACE ( 'NONE', ( #6330 ), #12064, .F. ) ;
#11191=DIRECTION ( 'NONE',  ( 0.000000000000000000, 0.000000000000000000, 1.000000000000000000 ) ) ;
#11194=CIRCLE ( 'NONE', #16581, 2.700000000000000622 ) ;
#11207=AXIS2_PLACEMENT_3D ( 'NONE', #18946, #4347, #20635 ) ;
#11210=AXIS2_PLACEMENT_3D ( 'NONE', #9473, #14914, #3769 ) ;
#11261=CARTESIAN_POINT ( 'NONE',  ( 0.000000000000000000, -2.357898499370432610, 3.252606517456513302E-15 ) ) ;
#11280=CARTESIAN_POINT ( 'NONE',  ( 0.000000000000000000, 0.000000000000000000, 0.000000000000000000 ) ) ;
#11282=EDGE_CURVE ( 'NONE', #11372, #19431, #14752, .T. ) ;
#11285=PRESENTATION_STYLE_ASSIGNMENT (( #9084 ) ) ;
#11319=TOROIDAL_SURFACE ( 'NONE', #20918, 4.000000000000000000, 0.2500000000000000000 ) ;
#11330=CARTESIAN_POINT ( 'NONE',  ( 2.500000000000000000, 0.000000000000000000, 0.000000000000000000 ) ) ;
#11336=AXIS2_PLACEMENT_3D ( 'NONE', #21700, #5158, #10873 ) ;
#11351=DIRECTION ( 'NONE',  ( -1.000000000000000000, -0.000000000000000000, -0.000000000000000000 ) ) ;
#11359=DIRECTION ( 'NONE',  ( 0.000000000000000000, 0.000000000000000000, 1.000000000000000000 ) ) ;
#11360=VECTOR ( 'NONE', #5424, 1000.000000000000114 ) ;
#11372=VERTEX_POINT ( 'NONE', #1930 ) ;
#11422=FACE_OUTER_BOUND ( 'NONE', #23344, .T. ) ;
#11435=ORIENTED_EDGE ( 'NONE', *, *, #15826, .F. ) ;
#11460=DIRECTION ( 'NONE',  ( -1.000000000000000000, -0.000000000000000000, -0.000000000000000000 ) ) ;
#11494=ADVANCED_FACE ( 'NONE', ( #13085 ), #12134, .T. ) ;
#11556=ORIENTED_EDGE ( 'NONE', *, *, #5291, .T. ) ;
#11569=CIRCLE ( 'NONE', #4201, 0.2500000000000002220 ) ;
#11607=DIRECTION ( 'NONE',  ( 1.000000000000000000, 0.000000000000000000, 0.000000000000000000 ) ) ;
#11620=AXIS2_PLACEMENT_3D ( 'NONE', #20449, #5845, #18739 ) ;
#11621=DIRECTION ( 'NONE',  ( -1.000000000000000000, -0.000000000000000000, -0.000000000000000000 ) ) ;
#11649=ORIENTED_EDGE ( 'NONE', *, *, #18345, .T. ) ;
#11650=DIRECTION ( 'NONE',  ( 1.000000000000000000, 0.000000000000000000, 0.000000000000000000 ) ) ;
#11728=VECTOR ( 'NONE', #7462, 1000.000000000000000 ) ;
#11731=EDGE_CURVE ( 'NONE', #12943, #6907, #21951, .T. ) ;
#11741=CIRCLE ( 'NONE', #11336, 2.041999999999999815 ) ;
#11768=VECTOR ( 'NONE', #9133, 1000.000000000000000 ) ;
#11770=AXIS2_PLACEMENT_3D ( 'NONE', #282, #7519, #1837 ) ;
#11807=DIRECTION ( 'NONE',  ( 1.000000000000000000, 0.000000000000000000, 0.000000000000000000 ) ) ;
#11816=EDGE_CURVE ( 'NONE', #8393, #21826, #148, .T. ) ;
#11855=EDGE_LOOP ( 'NONE', ( #4953, #13125, #1437, #17303 ) ) ;
#11930=VERTEX_POINT ( 'NONE', #4321 ) ;
#11969=ORIENTED_EDGE ( 'NONE', *, *, #18351, .T. ) ;
#12040=DIRECTION ( 'NONE',  ( 1.000000000000000000, 0.000000000000000000, 0.000000000000000000 ) ) ;
#12041=ADVANCED_FACE ( 'NONE', ( #21693 ), #10498, .T. ) ;
#12064=PLANE ( 'NONE',  #1329 ) ;
#12102=AXIS2_PLACEMENT_3D ( 'NONE', #15450, #2247, #9761 ) ;
#12106=CARTESIAN_POINT ( 'NONE',  ( 2.500000000000000000, 2.357898499370433054, -1.951563910473907981E-15 ) ) ;
#12125=EDGE_CURVE ( 'NONE', #9739, #15982, #14818, .T. ) ;
#12134=TOROIDAL_SURFACE ( 'NONE', #5165, 4.000000000000000000, 0.2500000000000000000 ) ;
#12142=PLANE ( 'NONE',  #10754 ) ;
#12144=ORIENTED_EDGE ( 'NONE', *, *, #7701, .F. ) ;
#12147=AXIS2_PLACEMENT_3D ( 'NONE', #3232, #17982, #9300 ) ;
#12150=ORIENTED_EDGE ( 'NONE', *, *, #10670, .T. ) ;
#12160=EDGE_LOOP ( 'NONE', ( #5906, #17247, #22055, #2707 ) ) ;
#12167=CARTESIAN_POINT ( 'NONE',  ( 2.500000000000000000, -1.178949249685213863, 2.042000000000002924 ) ) ;
#12177=( NAMED_UNIT ( * ) PLANE_ANGLE_UNIT ( ) SI_UNIT ( $, .RADIAN. ) );
#12237=VECTOR ( 'NONE', #17325, 1000.000000000000114 ) ;
#12245=EDGE_LOOP ( 'NONE', ( #9860, #17059, #1669, #7251, #16058 ) ) ;
#12264=EDGE_LOOP ( 'NONE', ( #3033, #3249, #14672, #5877, #2847 ) ) ;
#12266=CIRCLE ( 'NONE', #9148, 2.055000000000000160 ) ;
#12363=( GEOMETRIC_REPRESENTATION_CONTEXT ( 3 ) GLOBAL_UNCERTAINTY_ASSIGNED_CONTEXT ( ( #6303 ) ) GLOBAL_UNIT_ASSIGNED_CONTEXT ( ( #13864, #12177, #10336 ) ) REPRESENTATION_CONTEXT ( 'NONE', 'WORKASPACE' ) );
#12366=AXIS2_PLACEMENT_3D ( 'NONE', #5981, #13164, #18538 ) ;
#12380=EDGE_CURVE ( 'NONE', #7788, #1816, #14796, .T. ) ;
#12413=VERTEX_POINT ( 'NONE', #14206 ) ;
#12420=CARTESIAN_POINT ( 'NONE',  ( 17.00000000000000000, 2.516649172247811061E-16, -2.055000000000000160 ) ) ;
#12437=EDGE_CURVE ( 'NONE', #12943, #1821, #1138, .T. ) ;
#12508=FACE_OUTER_BOUND ( 'NONE', #16185, .T. ) ;
#12521=DIRECTION ( 'NONE',  ( -1.000000000000000000, -0.000000000000000000, -0.000000000000000000 ) ) ;
#12524=CARTESIAN_POINT ( 'NONE',  ( 2.500000000000000000, -2.629050547790028551E-15, -2.041999999999999815 ) ) ;
#12595=AXIS2_PLACEMENT_3D ( 'NONE', #23283, #22811, #14033 ) ;
#12680=CARTESIAN_POINT ( 'NONE',  ( 5.200000000000002842, 3.061616997868383634E-16, -2.500000000000000444 ) ) ;
#12687=AXIS2_PLACEMENT_3D ( 'NONE', #18152, #6916, #7259 ) ;
#12722=CIRCLE ( 'NONE', #2248, 4.000000000000000000 ) ;
#12760=VECTOR ( 'NONE', #15060, 1000.000000000000114 ) ;
#12762=EDGE_LOOP ( 'NONE', ( #804, #5495 ) ) ;
#12775=EDGE_CURVE ( 'NONE', #14717, #1127, #21743, .T. ) ;
#12821=PLANE ( 'NONE',  #15041 ) ;
#12825=VERTEX_POINT ( 'NONE', #12680 ) ;
#12863=EDGE_LOOP ( 'NONE', ( #17685, #20891, #14036 ) ) ;
#12879=VERTEX_POINT ( 'NONE', #9139 ) ;
#12900=CARTESIAN_POINT ( 'NONE',  ( 2.500000000000000000, -2.357898499370432610, 3.252606517456513302E-15 ) ) ;
#12943=VERTEX_POINT ( 'NONE', #5625 ) ;
#12966=DIRECTION ( 'NONE',  ( -0.7071067811865369146, 8.659560562355062281E-17, -0.7071067811865582309 ) ) ;
#12990=VECTOR ( 'NONE', #8302, 1000.000000000000114 ) ;
#13027=DIRECTION ( 'NONE',  ( 0.000000000000000000, 0.000000000000000000, -1.000000000000000000 ) ) ;
#13039=VECTOR ( 'NONE', #7467, 1000.000000000000000 ) ;
#13059=VECTOR ( 'NONE', #3166, 999.9999999999998863 ) ;
#13085=FACE_OUTER_BOUND ( 'NONE', #18646, .T. ) ;
#13091=VECTOR ( 'NONE', #17703, 1000.000000000000114 ) ;
#13125=ORIENTED_EDGE ( 'NONE', *, *, #20664, .T. ) ;
#13136=CARTESIAN_POINT ( 'NONE',  ( 2.500000000000000000, 2.357898499370433054, -1.951563910473907981E-15 ) ) ;
#13164=DIRECTION ( 'NONE',  ( -1.000000000000000000, -0.000000000000000000, -0.000000000000000000 ) ) ;
#13187=ORIENTED_EDGE ( 'NONE', *, *, #17688, .T. ) ;
#13221=CARTESIAN_POINT ( 'NONE',  ( 0.000000000000000000, -2.357898499370432610, 3.252606517456513302E-15 ) ) ;
#13284=CARTESIAN_POINT ( 'NONE',  ( 2.500000000000000000, 0.000000000000000000, 0.000000000000000000 ) ) ;
#13382=ADVANCED_FACE ( 'NONE', ( #11422 ), #5840, .F. ) ;
#13420=DIRECTION ( 'NONE',  ( 0.000000000000000000, 0.000000000000000000, 1.000000000000000000 ) ) ;
#13425=CARTESIAN_POINT ( 'NONE',  ( 2.500000000000000000, 0.000000000000000000, 0.000000000000000000 ) ) ;
#13433=CARTESIAN_POINT ( 'NONE',  ( 17.00000000000000000, 0.000000000000000000, 0.000000000000000000 ) ) ;
#13437=AXIS2_PLACEMENT_3D ( 'NONE', #2048, #11650, #5820 ) ;
#13443=PLANE ( 'NONE',  #11207 ) ;
#13455=PLANE ( 'NONE',  #13437 ) ;
#13456=VECTOR ( 'NONE', #12521, 1000.000000000000000 ) ;
#13525=CARTESIAN_POINT ( 'NONE',  ( 2.500000000000000000, 0.000000000000000000, 0.000000000000000000 ) ) ;
#13542=VECTOR ( 'NONE', #8028, 1000.000000000000000 ) ;
#13551=CARTESIAN_POINT ( 'NONE',  ( 16.55500000000001393, 0.000000000000000000, 2.500000000000000444 ) ) ;
#13553=UNCERTAINTY_MEASURE_WITH_UNIT (LENGTH_MEASURE( 1.000000000000000082E-05 ), #9334, 'distance_accuracy_value', 'NONE');
#13555=VERTEX_POINT ( 'NONE', #10086 ) ;
#13589=CYLINDRICAL_SURFACE ( 'NONE', #7590, 2.500000000000000444 ) ;
#13651=CIRCLE ( 'NONE', #866, 4.250000000000000000 ) ;
#13780=CARTESIAN_POINT ( 'NONE',  ( 16.55500000000001393, 0.000000000000000000, 0.000000000000000000 ) ) ;
#13825=EDGE_CURVE ( 'NONE', #10912, #874, #12722, .T. ) ;
#13864=( LENGTH_UNIT ( ) NAMED_UNIT ( * ) SI_UNIT ( .MILLI., .METRE. ) );
#13878=ORIENTED_EDGE ( 'NONE', *, *, #7837, .F. ) ;
#13883=CIRCLE ( 'NONE', #16551, 4.250000000000000000 ) ;
#13894=CARTESIAN_POINT ( 'NONE',  ( 2.500000000000000000, -1.768423874527823569, 1.021000000000002794 ) ) ;
#13946=EDGE_CURVE ( 'NONE', #11930, #18385, #23791, .T. ) ;
#14033=DIRECTION ( 'NONE',  ( 0.000000000000000000, -1.000000000000000000, 1.471414886128461471E-15 ) ) ;
#14036=ORIENTED_EDGE ( 'NONE', *, *, #6456, .F. ) ;
#14077=CARTESIAN_POINT ( 'NONE',  ( 2.500000000000000000, -1.178949249685213863, 2.042000000000002924 ) ) ;
#14107=DIRECTION ( 'NONE',  ( 0.000000000000000000, -1.000000000000000000, 0.000000000000000000 ) ) ;
#14206=CARTESIAN_POINT ( 'NONE',  ( 3.678949249685231848, 5.299604027854762026E-17, 0.000000000000000000 ) ) ;
#14238=AXIS2_PLACEMENT_3D ( 'NONE', #23515, #23259, #1044 ) ;
#14283=AXIS2_PLACEMENT_3D ( 'NONE', #13136, #1969, #3900 ) ;
#14378=FACE_OUTER_BOUND ( 'NONE', #11855, .T. ) ;
#14412=DIRECTION ( 'NONE',  ( 0.000000000000000000, 0.4999999999999993894, -0.8660254037844389297 ) ) ;
#14446=CARTESIAN_POINT ( 'NONE',  ( 0.000000000000000000, 1.178949249685213863, -2.042000000000001148 ) ) ;
#14599=EDGE_CURVE ( 'NONE', #12943, #23173, #10144, .T. ) ;
#14672=ORIENTED_EDGE ( 'NONE', *, *, #11731, .T. ) ;
#14704=EDGE_LOOP ( 'NONE', ( #6015, #20046, #7375, #22810 ) ) ;
#14717=VERTEX_POINT ( 'NONE', #16505 ) ;
#14752=LINE ( 'NONE', #12420, #10624 ) ;
#14794=PLANE ( 'NONE',  #14283 ) ;
#14796=CIRCLE ( 'NONE', #4767, 4.250000000000000000 ) ;
#14809=ADVANCED_FACE ( 'NONE', ( #21927 ), #12821, .T. ) ;
#14814=ORIENTED_EDGE ( 'NONE', *, *, #9357, .F. ) ;
#14818=LINE ( 'NONE', #5617, #11768 ) ;
#14838=EDGE_CURVE ( 'NONE', #3845, #13555, #21198, .T. ) ;
#14859=ORIENTED_EDGE ( 'NONE', *, *, #17878, .F. ) ;
#14872=ORIENTED_EDGE ( 'NONE', *, *, #3797, .T. ) ;
#14883=( NAMED_UNIT ( * ) PLANE_ANGLE_UNIT ( ) SI_UNIT ( $, .RADIAN. ) );
#14889=DIRECTION ( 'NONE',  ( 0.000000000000000000, 0.000000000000000000, -1.000000000000000000 ) ) ;
#14914=DIRECTION ( 'NONE',  ( 0.000000000000000000, 0.000000000000000000, 1.000000000000000000 ) ) ;
#14946=DIRECTION ( 'NONE',  ( 0.000000000000000000, 0.000000000000000000, -1.000000000000000000 ) ) ;
#15004=CARTESIAN_POINT ( 'NONE',  ( 5.000000000000002665, 0.000000000000000000, -2.700000000000000622 ) ) ;
#15038=VECTOR ( 'NONE', #19605, 999.9999999999998863 ) ;
#15041=AXIS2_PLACEMENT_3D ( 'NONE', #1414, #3568, #3338 ) ;
#15047=EDGE_CURVE ( 'NONE', #12879, #8456, #23125, .T. ) ;
#15060=DIRECTION ( 'NONE',  ( -0.5000000000000051070, 1.060575238724903217E-16, -0.8660254037844355990 ) ) ;
#15137=ORIENTED_EDGE ( 'NONE', *, *, #14838, .F. ) ;
#15331=CARTESIAN_POINT ( 'NONE',  ( 2.500000000000000000, 1.768423874527822681, -1.021000000000002794 ) ) ;
#15365=DIRECTION ( 'NONE',  ( 0.000000000000000000, 0.000000000000000000, -1.000000000000000000 ) ) ;
#15413=FACE_OUTER_BOUND ( 'NONE', #14704, .T. ) ;
#15434=ORIENTED_EDGE ( 'NONE', *, *, #9516, .F. ) ;
#15450=CARTESIAN_POINT ( 'NONE',  ( 5.200000000000002842, 0.000000000000000000, 0.000000000000000000 ) ) ;
#15466=DIRECTION ( 'NONE',  ( -1.000000000000000000, -0.000000000000000000, -0.000000000000000000 ) ) ;
#15509=DIRECTION ( 'NONE',  ( 0.000000000000000000, 0.4999999999999993339, -0.8660254037844390407 ) ) ;
#15580=EDGE_LOOP ( 'NONE', ( #8062, #6162, #17326, #9415, #16334 ) ) ;
#15588=ADVANCED_FACE ( 'NONE', ( #23449 ), #9090, .T. ) ;
#15627=ORIENTED_EDGE ( 'NONE', *, *, #14599, .F. ) ;
#15655=EDGE_CURVE ( 'NONE', #2537, #12825, #4540, .T. ) ;
#15679=PLANE ( 'NONE',  #4843 ) ;
#15822=EDGE_CURVE ( 'NONE', #1821, #15982, #23399, .T. ) ;
#15826=EDGE_CURVE ( 'NONE', #18385, #19431, #17645, .T. ) ;
#15899=CARTESIAN_POINT ( 'NONE',  ( 0.000000000000000000, 2.357898499370433054, -1.951563910473907981E-15 ) ) ;
#15903=DIRECTION ( 'NONE',  ( 0.000000000000000000, 1.000000000000000000, -1.471414886128461471E-15 ) ) ;
#15941=PLANE ( 'NONE',  #12595 ) ;
#15982=VERTEX_POINT ( 'NONE', #682 ) ;
#16009=ADVANCED_FACE ( 'NONE', ( #9511 ), #23055, .F. ) ;
#16058=ORIENTED_EDGE ( 'NONE', *, *, #8667, .T. ) ;
#16158=ORIENTED_EDGE ( 'NONE', *, *, #10484, .T. ) ;
#16167=MECHANICAL_DESIGN_GEOMETRIC_PRESENTATION_REPRESENTATION('',(#23524),#3423);
#16179=AXIS2_PLACEMENT_3D ( 'NONE', #10492, #17827, #6963 ) ;
#16185=EDGE_LOOP ( 'NONE', ( #5578, #11969, #8291, #23063 ) ) ;
#16210=VECTOR ( 'NONE', #17600, 999.9999999999998863 ) ;
#16220=CARTESIAN_POINT ( 'NONE',  ( 2.500000000000000000, 1.178949249685218525, 2.041999999999999371 ) ) ;
#16289=CARTESIAN_POINT ( 'NONE',  ( 2.500000000000000000, 0.000000000000000000, 0.000000000000000000 ) ) ;
#16334=ORIENTED_EDGE ( 'NONE', *, *, #23025, .T. ) ;
#16409=PRODUCT_DEFINITION ( 'UNKNOWN', '', #20823, #11017 ) ;
#16468=DIRECTION ( 'NONE',  ( 1.000000000000000000, 0.000000000000000000, 0.000000000000000000 ) ) ;
#16486=DIRECTION ( 'NONE',  ( 1.000000000000000000, 0.000000000000000000, 0.000000000000000000 ) ) ;
#16505=CARTESIAN_POINT ( 'NONE',  ( 0.2500000000000002220, 0.000000000000000000, 4.250000000000000000 ) ) ;
#16526=EDGE_LOOP ( 'NONE', ( #9734, #627, #15137 ) ) ;
#16551=AXIS2_PLACEMENT_3D ( 'NONE', #9113, #16468, #11191 ) ;
#16581=AXIS2_PLACEMENT_3D ( 'NONE', #2089, #2204, #6079 ) ;
#16608=EDGE_CURVE ( 'NONE', #12879, #3080, #2916, .T. ) ;
#16686=FILL_AREA_STYLE ('',( #5687 ) ) ;
#16724=CARTESIAN_POINT ( 'NONE',  ( 0.000000000000000000, 5.051668046482832750E-16, -4.000000000000000000 ) ) ;
#16868=CARTESIAN_POINT ( 'NONE',  ( 5.000000000000004441, 5.204748896376250699E-16, -4.250000000000000000 ) ) ;
#16969=VECTOR ( 'NONE', #5049, 1000.000000000000114 ) ;
#17006=ORIENTED_EDGE ( 'NONE', *, *, #20041, .T. ) ;
#17014=DIRECTION ( 'NONE',  ( -1.000000000000000000, -0.000000000000000000, -0.000000000000000000 ) ) ;
#17030=DIRECTION ( 'NONE',  ( -1.000000000000000000, -0.000000000000000000, -0.000000000000000000 ) ) ;
#17059=ORIENTED_EDGE ( 'NONE', *, *, #1871, .T. ) ;
#17171=EDGE_CURVE ( 'NONE', #11372, #11930, #12266, .T. ) ;
#17247=ORIENTED_EDGE ( 'NONE', *, *, #17171, .T. ) ;
#17253=LINE ( 'NONE', #4562, #5744 ) ;
#17275=FACE_BOUND ( 'NONE', #3109, .T. ) ;
#17303=ORIENTED_EDGE ( 'NONE', *, *, #10484, .F. ) ;
#17325=DIRECTION ( 'NONE',  ( 0.000000000000000000, -0.5000000000000011102, -0.8660254037844379305 ) ) ;
#17326=ORIENTED_EDGE ( 'NONE', *, *, #16608, .T. ) ;
#17331=ORIENTED_EDGE ( 'NONE', *, *, #6643, .F. ) ;
#17334=STYLED_ITEM('',(#23927),#20059);
#17365=COLOUR_RGB ( '',1.000000000000000000, 0.9490196078431372140, 0.9098039215686274384 ) ;
#17378=DIRECTION ( 'NONE',  ( 0.000000000000000000, 0.000000000000000000, 1.000000000000000000 ) ) ;
#17384=VECTOR ( 'NONE', #15903, 1000.000000000000000 ) ;
#17464=VECTOR ( 'NONE', #15466, 1000.000000000000000 ) ;
#17476=LINE ( 'NONE', #920, #12990 ) ;
#17600=DIRECTION ( 'NONE',  ( 0.000000000000000000, -0.5000000000000012212, -0.8660254037844380415 ) ) ;
#17625=CIRCLE ( 'NONE', #22638, 2.041999999999999815 ) ;
#17643=FACE_OUTER_BOUND ( 'NONE', #20111, .T. ) ;
#17645=CIRCLE ( 'NONE', #5313, 2.500000000000000444 ) ;
#17657=VECTOR ( 'NONE', #3306, 1000.000000000000000 ) ;
#17685=ORIENTED_EDGE ( 'NONE', *, *, #11731, .F. ) ;
#17688=EDGE_CURVE ( 'NONE', #23173, #20673, #2342, .T. ) ;
#17702=AXIS2_PLACEMENT_3D ( 'NONE', #23242, #14107, #1158 ) ;
#17703=DIRECTION ( 'NONE',  ( -0.5000000000000051070, 0.000000000000000000, 0.8660254037844355990 ) ) ;
#17811=DIRECTION ( 'NONE',  ( 0.000000000000000000, 0.000000000000000000, 1.000000000000000000 ) ) ;
#17827=DIRECTION ( 'NONE',  ( -1.000000000000000000, -0.000000000000000000, -0.000000000000000000 ) ) ;
#17878=EDGE_CURVE ( 'NONE', #19431, #12825, #3629, .T. ) ;
#17892=FACE_OUTER_BOUND ( 'NONE', #12264, .T. ) ;
#17949=DIRECTION ( 'NONE',  ( -1.000000000000000000, -0.000000000000000000, -0.000000000000000000 ) ) ;
#17952=DIRECTION ( 'NONE',  ( 0.000000000000000000, 0.000000000000000000, 1.000000000000000000 ) ) ;
#17953=ORIENTED_EDGE ( 'NONE', *, *, #12125, .T. ) ;
#17958=CARTESIAN_POINT ( 'NONE',  ( 2.500000000000000000, 1.178949249685213863, -2.042000000000001148 ) ) ;
#17961=CARTESIAN_POINT ( 'NONE',  ( 5.000000000000000888, 4.250000000000000000, 0.000000000000000000 ) ) ;
#17976=ORIENTED_EDGE ( 'NONE', *, *, #18746, .T. ) ;
#17982=DIRECTION ( 'NONE',  ( -1.000000000000000000, -0.000000000000000000, -0.000000000000000000 ) ) ;
#18067=DIRECTION ( 'NONE',  ( 0.000000000000000000, 0.000000000000000000, 1.000000000000000000 ) ) ;
#18083=SHAPE_REPRESENTATION ( 'socket head cap screw_iso_ISO 4762 M5 x 12 - 12N', ( #11210 ), #3838 ) ;
#18131=PLANE ( 'NONE',  #23701 ) ;
#18152=CARTESIAN_POINT ( 'NONE',  ( 2.500000000000000000, -1.178949249685213863, 2.042000000000002924 ) ) ;
#18226=LINE ( 'NONE', #11261, #13039 ) ;
#18332=DIRECTION ( 'NONE',  ( -1.000000000000000000, -0.000000000000000000, -0.000000000000000000 ) ) ;
#18345=EDGE_CURVE ( 'NONE', #20673, #2323, #22297, .T. ) ;
#18350=DIRECTION ( 'NONE',  ( 0.000000000000000000, 0.000000000000000000, 1.000000000000000000 ) ) ;
#18351=EDGE_CURVE ( 'NONE', #1816, #1127, #2498, .T. ) ;
#18369=ORIENTED_EDGE ( 'NONE', *, *, #18746, .F. ) ;
#18385=VERTEX_POINT ( 'NONE', #13551 ) ;
#18399=LINE ( 'NONE', #18631, #12760 ) ;
#18413=FACE_BOUND ( 'NONE', #6635, .T. ) ;
#18444=LINE ( 'NONE', #22308, #3776 ) ;
#18451=ADVANCED_FACE ( 'NONE', ( #578 ), #6004, .F. ) ;
#18484=DIRECTION ( 'NONE',  ( -0.000000000000000000, 1.000000000000000000, 1.224646799147353207E-16 ) ) ;
#18486=( LENGTH_UNIT ( ) NAMED_UNIT ( * ) SI_UNIT ( .MILLI., .METRE. ) );
#18538=DIRECTION ( 'NONE',  ( 0.000000000000000000, 0.000000000000000000, 1.000000000000000000 ) ) ;
#18550=DIRECTION ( 'NONE',  ( 0.000000000000000000, 0.000000000000000000, -1.000000000000000000 ) ) ;
#18596=ORIENTED_EDGE ( 'NONE', *, *, #11816, .F. ) ;
#18614=EDGE_CURVE ( 'NONE', #9739, #6820, #17476, .T. ) ;
#18616=ADVANCED_FACE ( 'NONE', ( #2956 ), #15679, .F. ) ;
#18631=CARTESIAN_POINT ( 'NONE',  ( 2.500000000000000000, 2.500728763858895382E-16, -2.041999999999999815 ) ) ;
#18639=DIRECTION ( 'NONE',  ( 0.000000000000000000, 0.000000000000000000, 1.000000000000000000 ) ) ;
#18646=EDGE_LOOP ( 'NONE', ( #6290, #22670, #6509, #8904 ) ) ;
#18674=FACE_OUTER_BOUND ( 'NONE', #19906, .T. ) ;
#18737=ADVANCED_FACE ( 'NONE', ( #10966 ), #2142, .F. ) ;
#18739=DIRECTION ( 'NONE',  ( 0.000000000000000000, 0.000000000000000000, 1.000000000000000000 ) ) ;
#18746=EDGE_CURVE ( 'NONE', #13555, #3080, #9093, .T. ) ;
#18883=CIRCLE ( 'NONE', #8496, 2.055000000000000160 ) ;
#18886=ORIENTED_EDGE ( 'NONE', *, *, #7564, .F. ) ;
#18909=AXIS2_PLACEMENT_3D ( 'NONE', #13780, #21455, #17378 ) ;
#18911=EDGE_LOOP ( 'NONE', ( #13187, #22510, #20123 ) ) ;
#18946=CARTESIAN_POINT ( 'NONE',  ( 0.000000000000000000, 0.000000000000000000, 0.000000000000000000 ) ) ;
#19010=DIRECTION ( 'NONE',  ( 0.000000000000000000, -1.000000000000000000, 0.000000000000000000 ) ) ;
#19011=ORIENTED_EDGE ( 'NONE', *, *, #16608, .F. ) ;
#19041=AXIS2_PLACEMENT_3D ( 'NONE', #10969, #1401, #17952 ) ;
#19061=DIRECTION ( 'NONE',  ( 0.000000000000000000, 0.000000000000000000, 1.000000000000000000 ) ) ;
#19169=ORIENTED_EDGE ( 'NONE', *, *, #17688, .F. ) ;
#19188=EDGE_CURVE ( 'NONE', #20673, #3845, #9322, .T. ) ;
#19220=VECTOR ( 'NONE', #6588, 1000.000000000000000 ) ;
#19288=ADVANCED_FACE ( 'NONE', ( #17275, #6163 ), #13443, .T. ) ;
#19397=ORIENTED_EDGE ( 'NONE', *, *, #23771, .F. ) ;
#19431=VERTEX_POINT ( 'NONE', #3705 ) ;
#19547=APPLICATION_CONTEXT ( 'automotive_design' ) ;
#19588=EDGE_LOOP ( 'NONE', ( #1730, #8971, #21482, #17976, #23429 ) ) ;
#19605=DIRECTION ( 'NONE',  ( 0.000000000000000000, -0.5000000000000012212, -0.8660254037844380415 ) ) ;
#19614=ORIENTED_EDGE ( 'NONE', *, *, #5291, .F. ) ;
#19629=VECTOR ( 'NONE', #20407, 1000.000000000000000 ) ;
#19641=DIRECTION ( 'NONE',  ( 1.000000000000000000, 0.000000000000000000, 0.000000000000000000 ) ) ;
#19673=CONICAL_SURFACE ( 'NONE', #3860, 2.055000000000000160, 0.7853981633974633780 ) ;
#19695=EDGE_CURVE ( 'NONE', #6907, #10894, #4916, .T. ) ;
#19818=DIRECTION ( 'NONE',  ( -1.000000000000000000, -0.000000000000000000, -0.000000000000000000 ) ) ;
#19858=LINE ( 'NONE', #14446, #17657 ) ;
#19881=DIRECTION ( 'NONE',  ( 0.000000000000000000, 0.000000000000000000, -1.000000000000000000 ) ) ;
#19906=EDGE_LOOP ( 'NONE', ( #3362, #8400, #10242, #13878 ) ) ;
#19926=DIRECTION ( 'NONE',  ( -1.000000000000000000, -0.000000000000000000, -0.000000000000000000 ) ) ;
#20041=EDGE_CURVE ( 'NONE', #8456, #10894, #5016, .T. ) ;
#20046=ORIENTED_EDGE ( 'NONE', *, *, #7564, .T. ) ;
#20059=MANIFOLD_SOLID_BREP ( 'Hex', #20629 ) ;
#20061=DIRECTION ( 'NONE',  ( -1.000000000000000000, -0.000000000000000000, -0.000000000000000000 ) ) ;
#20064=DIRECTION ( 'NONE',  ( 0.000000000000000000, -1.224646799147353454E-16, 1.000000000000000000 ) ) ;
#20107=ORIENTED_EDGE ( 'NONE', *, *, #12125, .F. ) ;
#20111=EDGE_LOOP ( 'NONE', ( #19011, #21268, #15434 ) ) ;
#20123=ORIENTED_EDGE ( 'NONE', *, *, #8667, .F. ) ;
#20177=VECTOR ( 'NONE', #10703, 1000.000000000000000 ) ;
#20326=ORIENTED_EDGE ( 'NONE', *, *, #15822, .T. ) ;
#20342=VECTOR ( 'NONE', #4360, 1000.000000000000114 ) ;
#20353=ADVANCED_FACE ( 'NONE', ( #17643 ), #12142, .F. ) ;
#20404=DIRECTION ( 'NONE',  ( -1.000000000000000000, -0.000000000000000000, -0.000000000000000000 ) ) ;
#20407=DIRECTION ( 'NONE',  ( -0.7071067811865369146, 0.000000000000000000, 0.7071067811865582309 ) ) ;
#20411=( NAMED_UNIT ( * ) SI_UNIT ( $, .STERADIAN. ) SOLID_ANGLE_UNIT ( ) );
#20449=CARTESIAN_POINT ( 'NONE',  ( 2.500000000000000000, 0.000000000000000000, 0.000000000000000000 ) ) ;
#20461=ORIENTED_EDGE ( 'NONE', *, *, #8482, .F. ) ;
#20490=CARTESIAN_POINT ( 'NONE',  ( 2.500000000000000000, 1.178949249685213863, -2.042000000000001148 ) ) ;
#20592=DIRECTION ( 'NONE',  ( 0.000000000000000000, 0.000000000000000000, 1.000000000000000000 ) ) ;
#20629=CLOSED_SHELL ( 'NONE', ( #22232, #7529, #9931, #6663, #8280, #3506, #19288, #4286, #6049, #12041, #7729, #4851, #18737, #11494, #6570, #4554, #15588, #14809, #13382, #5054, #18616, #616, #20353, #21798, #11182, #18451, #16009 ) ) ;
#20630=ORIENTED_EDGE ( 'NONE', *, *, #15047, .F. ) ;
#20635=DIRECTION ( 'NONE',  ( -0.000000000000000000, 0.000000000000000000, 1.000000000000000000 ) ) ;
#20664=EDGE_CURVE ( 'NONE', #2537, #8393, #9985, .T. ) ;
#20673=VERTEX_POINT ( 'NONE', #17958 ) ;
#20708=CARTESIAN_POINT ( 'NONE',  ( 0.2500000000000002220, 0.000000000000000000, 4.000000000000000000 ) ) ;
#20715=EDGE_LOOP ( 'NONE', ( #17953, #17331, #21763, #20630, #14872 ) ) ;
#20728=UNCERTAINTY_MEASURE_WITH_UNIT (LENGTH_MEASURE( 1.000000000000000082E-05 ), #18486, 'distance_accuracy_value', 'NONE');
#20747=DIRECTION ( 'NONE',  ( 0.000000000000000000, 0.000000000000000000, 1.000000000000000000 ) ) ;
#20771=FACE_OUTER_BOUND ( 'NONE', #23555, .T. ) ;
#20823=PRODUCT_DEFINITION_FORMATION_WITH_SPECIFIED_SOURCE ( 'ANY', '', #10988, .NOT_KNOWN. ) ;
#20891=ORIENTED_EDGE ( 'NONE', *, *, #14599, .T. ) ;
#20918=AXIS2_PLACEMENT_3D ( 'NONE', #230, #9529, #13420 ) ;
#20951=CARTESIAN_POINT ( 'NONE',  ( -31.74999999999995737, 0.000000000000000000, 0.000000000000000000 ) ) ;
#21008=ORIENTED_EDGE ( 'NONE', *, *, #6136, .T. ) ;
#21021=CARTESIAN_POINT ( 'NONE',  ( 0.000000000000000000, 2.357898499370433054, -1.951563910473907981E-15 ) ) ;
#21054=VECTOR ( 'NONE', #15509, 1000.000000000000000 ) ;
#21065=ORIENTED_EDGE ( 'NONE', *, *, #7494, .F. ) ;
#21069=CARTESIAN_POINT ( 'NONE',  ( 2.500000000000000000, -1.178949249685213863, 2.042000000000002924 ) ) ;
#21198=CIRCLE ( 'NONE', #6545, 2.041999999999999815 ) ;
#21224=CARTESIAN_POINT ( 'NONE',  ( 2.500000000000000000, 2.357898499370433054, -1.951563910473907981E-15 ) ) ;
#21268=ORIENTED_EDGE ( 'NONE', *, *, #15047, .T. ) ;
#21391=APPLICATION_CONTEXT ( 'automotive_design' ) ;
#21394=EDGE_CURVE ( 'NONE', #1127, #14717, #13883, .T. ) ;
#21411=CARTESIAN_POINT ( 'NONE',  ( 0.000000000000000000, 1.178949249685213863, -2.042000000000001148 ) ) ;
#21455=DIRECTION ( 'NONE',  ( -1.000000000000000000, -0.000000000000000000, -0.000000000000000000 ) ) ;
#21482=ORIENTED_EDGE ( 'NONE', *, *, #14838, .T. ) ;
#21497=ORIENTED_EDGE ( 'NONE', *, *, #20664, .F. ) ;
#21599=EDGE_CURVE ( 'NONE', #1127, #874, #11569, .T. ) ;
#21693=FACE_OUTER_BOUND ( 'NONE', #21953, .T. ) ;
#21700=CARTESIAN_POINT ( 'NONE',  ( 2.500000000000000000, 0.000000000000000000, 0.000000000000000000 ) ) ;
#21707=CARTESIAN_POINT ( 'NONE',  ( 5.200000000000002842, 0.000000000000000000, 0.000000000000000000 ) ) ;
#21743=CIRCLE ( 'NONE', #22888, 4.250000000000000000 ) ;
#21763=ORIENTED_EDGE ( 'NONE', *, *, #20041, .F. ) ;
#21798=ADVANCED_FACE ( 'NONE', ( #2167 ), #13455, .F. ) ;
#21826=VERTEX_POINT ( 'NONE', #15004 ) ;
#21891=ORIENTED_EDGE ( 'NONE', *, *, #7102, .T. ) ;
#21927=FACE_OUTER_BOUND ( 'NONE', #1713, .T. ) ;
#21951=LINE ( 'NONE', #1776, #11360 ) ;
#21953=EDGE_LOOP ( 'NONE', ( #14859, #21008, #3603, #4449 ) ) ;
#21991=EDGE_LOOP ( 'NONE', ( #2769, #18886 ) ) ;
#22055=ORIENTED_EDGE ( 'NONE', *, *, #13946, .T. ) ;
#22097=( NAMED_UNIT ( * ) PLANE_ANGLE_UNIT ( ) SI_UNIT ( $, .RADIAN. ) );
#22232=ADVANCED_FACE ( 'NONE', ( #3917 ), #23435, .F. ) ;
#22297=LINE ( 'NONE', #20490, #22552 ) ;
#22308=CARTESIAN_POINT ( 'NONE',  ( 2.500000000000000000, -2.357898499370432610, 3.252606517456513302E-15 ) ) ;
#22309=CARTESIAN_POINT ( 'NONE',  ( 5.000000000000004441, 0.000000000000000000, 0.000000000000000000 ) ) ;
#22456=CARTESIAN_POINT ( 'NONE',  ( 2.500000000000000000, 1.178949249685218525, 2.041999999999999371 ) ) ;
#22510=ORIENTED_EDGE ( 'NONE', *, *, #19188, .T. ) ;
#22552=VECTOR ( 'NONE', #17014, 1000.000000000000000 ) ;
#22558=DIRECTION ( 'NONE',  ( 0.000000000000000000, -1.000000000000000000, 1.287488025362403787E-15 ) ) ;
#22568=CARTESIAN_POINT ( 'NONE',  ( 0.000000000000000000, -1.178949249685218303, -2.041999999999998039 ) ) ;
#22575=VECTOR ( 'NONE', #22558, 1000.000000000000000 ) ;
#22623=DIRECTION ( 'NONE',  ( 0.000000000000000000, 0.000000000000000000, -1.000000000000000000 ) ) ;
#22638=AXIS2_PLACEMENT_3D ( 'NONE', #13425, #22907, #2627 ) ;
#22665=DIRECTION ( 'NONE',  ( 0.000000000000000000, 0.000000000000000000, 1.000000000000000000 ) ) ;
#22670=ORIENTED_EDGE ( 'NONE', *, *, #12775, .F. ) ;
#22683=CARTESIAN_POINT ( 'NONE',  ( 2.500000000000000000, 1.178949249685213863, -2.042000000000001148 ) ) ;
#22714=AXIS2_PLACEMENT_3D ( 'NONE', #8041, #4855, #14412 ) ;
#22769=DIRECTION ( 'NONE',  ( -1.000000000000000000, -0.000000000000000000, -0.000000000000000000 ) ) ;
#22810=ORIENTED_EDGE ( 'NONE', *, *, #12775, .T. ) ;
#22811=DIRECTION ( 'NONE',  ( -0.000000000000000000, 1.471414886128461471E-15, 1.000000000000000000 ) ) ;
#22888=AXIS2_PLACEMENT_3D ( 'NONE', #1641, #19641, #23623 ) ;
#22907=DIRECTION ( 'NONE',  ( -1.000000000000000000, -0.000000000000000000, -0.000000000000000000 ) ) ;
#22910=ORIENTED_EDGE ( 'NONE', *, *, #23771, .T. ) ;
#22953=AXIS2_PLACEMENT_3D ( 'NONE', #4155, #2217, #889 ) ;
#22977=CYLINDRICAL_SURFACE ( 'NONE', #22953, 4.250000000000000000 ) ;
#23025=EDGE_CURVE ( 'NONE', #10553, #6820, #18444, .T. ) ;
#23055=CONICAL_SURFACE ( 'NONE', #319, 2.041999999999999815, 1.047197551196591858 ) ;
#23063=ORIENTED_EDGE ( 'NONE', *, *, #4292, .F. ) ;
#23066=EDGE_CURVE ( 'NONE', #3080, #10553, #17253, .T. ) ;
#23125=LINE ( 'NONE', #8181, #17384 ) ;
#23173=VERTEX_POINT ( 'NONE', #15331 ) ;
#23242=CARTESIAN_POINT ( 'NONE',  ( 5.200000000000002842, 0.000000000000000000, -2.700000000000000622 ) ) ;
#23259=DIRECTION ( 'NONE',  ( 0.000000000000000000, 1.000000000000000000, -1.224646799147353207E-16 ) ) ;
#23271=DIRECTION ( 'NONE',  ( 1.000000000000000000, 0.000000000000000000, 0.000000000000000000 ) ) ;
#23283=CARTESIAN_POINT ( 'NONE',  ( 2.500000000000000000, -1.178949249685213863, 2.042000000000002924 ) ) ;
#23344=EDGE_LOOP ( 'NONE', ( #11048, #3635, #8877, #23792, #11649 ) ) ;
#23399=LINE ( 'NONE', #21021, #20342 ) ;
#23418=CARTESIAN_POINT ( 'NONE',  ( 5.000000000000002665, 3.306546357697854226E-16, 2.700000000000000622 ) ) ;
#23429=ORIENTED_EDGE ( 'NONE', *, *, #9516, .T. ) ;
#23435=CONICAL_SURFACE ( 'NONE', #7629, 2.041999999999999815, 1.047197551196591858 ) ;
#23437=PLANE ( 'NONE',  #22714 ) ;
#23448=CARTESIAN_POINT ( 'NONE',  ( 0.000000000000000000, -1.178949249685213863, 2.042000000000002924 ) ) ;
#23449=FACE_OUTER_BOUND ( 'NONE', #15580, .T. ) ;
#23515=CARTESIAN_POINT ( 'NONE',  ( 5.200000000000002842, 3.306546357697854226E-16, 2.700000000000000622 ) ) ;
#23524=STYLED_ITEM ( 'NONE', ( #11285 ), #7558 ) ;
#23555=EDGE_LOOP ( 'NONE', ( #11071, #2144, #21891, #21065 ) ) ;
#23562=LINE ( 'NONE', #21, #1332 ) ;
#23623=DIRECTION ( 'NONE',  ( 0.000000000000000000, 0.000000000000000000, 1.000000000000000000 ) ) ;
#23631=DIRECTION ( 'NONE',  ( -1.000000000000000000, -0.000000000000000000, -0.000000000000000000 ) ) ;
#23643=AXIS2_PLACEMENT_3D ( 'NONE', #20708, #19010, #14946 ) ;
#23699=CARTESIAN_POINT ( 'NONE',  ( 2.500000000000000000, 2.357898499370433054, -1.951563910473907981E-15 ) ) ;
#23701=AXIS2_PLACEMENT_3D ( 'NONE', #7373, #10911, #5207 ) ;
#23737=DIRECTION ( 'NONE',  ( 1.000000000000000000, 0.000000000000000000, 0.000000000000000000 ) ) ;
#23771=EDGE_CURVE ( 'NONE', #1821, #2323, #8528, .T. ) ;
#23791=LINE ( 'NONE', #7250, #19629 ) ;
#23792=ORIENTED_EDGE ( 'NONE', *, *, #19188, .F. ) ;
#23921=COLOUR_RGB('Black',0.12,0.14,0.17);
#23922=FILL_AREA_STYLE_COLOUR('',#23921);
#23923=FILL_AREA_STYLE('',(#23922));
#23924=SURFACE_STYLE_FILL_AREA(#23923);
#23925=SURFACE_SIDE_STYLE('',(#23924));
#23926=SURFACE_STYLE_USAGE(.BOTH.,#23925);
#23927=PRESENTATION_STYLE_ASSIGNMENT((#23926));
ENDSEC;
END-ISO-10303-21;
